ISO-10303-21;
HEADER;
FILE_DESCRIPTION (('STEP AP214'),
    '1' );
FILE_NAME ('Part9.step',
    '2026-11-01T05:08:46',
    ( '' ),
    ( '' ),
    'SwSTEP 2.0',
    'SolidWorks 2024',
    '' );
FILE_SCHEMA (( 'AUTOMOTIVE_DESIGN' ));
ENDSEC;

DATA;
#63=EDGE_LOOP ( 'NONE', ( #16636, #11334, #7139, #11945 ) ) ;
#105=ORIENTED_EDGE ( 'NONE', *, *, #15495, .F. ) ;
#114=AXIS2_PLACEMENT_3D ( 'NONE', #9847, #2332, #2672 ) ;
#165=ORIENTED_EDGE ( 'NONE', *, *, #15092, .T. ) ;
#184=CYLINDRICAL_SURFACE ( 'NONE', #9745, 5.268482129199949959 ) ;
#203=ORIENTED_EDGE ( 'NONE', *, *, #1323, .T. ) ;
#276=VERTEX_POINT ( 'NONE', #9787 ) ;
#366=AXIS2_PLACEMENT_3D ( 'NONE', #3740, #3651, #8892 ) ;
#374=ORIENTED_EDGE ( 'NONE', *, *, #4662, .T. ) ;
#386=VERTEX_POINT ( 'NONE', #6561 ) ;
#431=DIRECTION ( 'NONE',  ( -1.000000000000000000, -0.000000000000000000, -0.000000000000000000 ) ) ;
#468=ORIENTED_EDGE ( 'NONE', *, *, #16048, .T. ) ;
#549=( NAMED_UNIT ( * ) PLANE_ANGLE_UNIT ( ) SI_UNIT ( $, .RADIAN. ) );
#558=CIRCLE ( 'NONE', #16457, 4.000164074322309027 ) ;
#559=ORIENTED_EDGE ( 'NONE', *, *, #8857, .F. ) ;
#571=AXIS2_PLACEMENT_3D ( 'NONE', #3996, #14472, #2694 ) ;
#651=CYLINDRICAL_SURFACE ( 'NONE', #4039, 22.50000000000000000 ) ;
#655=DIRECTION ( 'NONE',  ( 0.000000000000000000, 0.000000000000000000, 1.000000000000000000 ) ) ;
#683=FACE_OUTER_BOUND ( 'NONE', #15993, .T. ) ;
#801=EDGE_CURVE ( 'NONE', #276, #14337, #9137, .T. ) ;
#816=LINE ( 'NONE', #15240, #16408 ) ;
#842=EDGE_CURVE ( 'NONE', #1983, #9375, #2545, .T. ) ;
#851=VERTEX_POINT ( 'NONE', #1149 ) ;
#917=DIRECTION ( 'NONE',  ( 0.000000000000000000, -1.224646799147352714E-16, 1.000000000000000000 ) ) ;
#944=AXIS2_PLACEMENT_3D ( 'NONE', #1343, #6564, #11817 ) ;
#989=TOROIDAL_SURFACE ( 'NONE', #7022, 22.46376988133006236, 4.000164074322307250 ) ;
#1029=EDGE_LOOP ( 'NONE', ( #11785, #8696, #16101, #13084 ) ) ;
#1032=FACE_OUTER_BOUND ( 'NONE', #15005, .T. ) ;
#1064=ORIENTED_EDGE ( 'NONE', *, *, #842, .F. ) ;
#1080=PRODUCT ( 'Part9', 'Part9', '', ( #1648 ) ) ;
#1113=EDGE_LOOP ( 'NONE', ( #9302, #15416, #3319, #4631 ) ) ;
#1149=CARTESIAN_POINT ( 'NONE',  ( -10.00000000000000000, 0.000000000000000000, -5.268482129199949959 ) ) ;
#1185=DIRECTION ( 'NONE',  ( -1.000000000000000000, -0.000000000000000000, -0.000000000000000000 ) ) ;
#1203=CIRCLE ( 'NONE', #11075, 5.268482129199949959 ) ;
#1253=CARTESIAN_POINT ( 'NONE',  ( 0.000000000000000000, 0.000000000000000000, -5.268482129199949959 ) ) ;
#1275=CARTESIAN_POINT ( 'NONE',  ( -5.000000000000000888, 0.000000000000000000, 22.46376988133006236 ) ) ;
#1278=ORIENTED_EDGE ( 'NONE', *, *, #9293, .T. ) ;
#1294=VERTEX_POINT ( 'NONE', #6413 ) ;
#1323=EDGE_CURVE ( 'NONE', #14799, #14337, #8320, .T. ) ;
#1343=CARTESIAN_POINT ( 'NONE',  ( -13.11912225705329327, 0.000000000000000000, 0.000000000000000000 ) ) ;
#1351=CARTESIAN_POINT ( 'NONE',  ( -9.000000000000001776, 0.000000000000000000, 0.000000000000000000 ) ) ;
#1467=PLANE ( 'NONE',  #4490 ) ;
#1477=VECTOR ( 'NONE', #8385, 1000.000000000000000 ) ;
#1482=AXIS2_PLACEMENT_3D ( 'NONE', #1275, #11751, #14075 ) ;
#1488=AXIS2_PLACEMENT_3D ( 'NONE', #3280, #8693, #15217 ) ;
#1622=CARTESIAN_POINT ( 'NONE',  ( -0.9999999999999991118, 0.000000000000000000, 0.000000000000000000 ) ) ;
#1641=VERTEX_POINT ( 'NONE', #13702 ) ;
#1648=PRODUCT_CONTEXT ( 'NONE', #7958, 'mechanical' ) ;
#1703=EDGE_CURVE ( 'NONE', #8258, #276, #816, .T. ) ;
#1708=DIRECTION ( 'NONE',  ( 0.000000000000000000, 0.000000000000000000, 1.000000000000000000 ) ) ;
#1750=( GEOMETRIC_REPRESENTATION_CONTEXT ( 3 ) GLOBAL_UNCERTAINTY_ASSIGNED_CONTEXT ( ( #6219 ) ) GLOBAL_UNIT_ASSIGNED_CONTEXT ( ( #14018, #549, #9750 ) ) REPRESENTATION_CONTEXT ( 'NONE', 'WORKASPACE' ) );
#1813=CARTESIAN_POINT ( 'NONE',  ( -10.00000000000000000, -1.224646799147353454E-15, 0.000000000000000000 ) ) ;
#1853=FACE_OUTER_BOUND ( 'NONE', #63, .T. ) ;
#1983=VERTEX_POINT ( 'NONE', #3440 ) ;
#2068=CIRCLE ( 'NONE', #10575, 5.268482129199949959 ) ;
#2096=CIRCLE ( 'NONE', #11697, 22.50000000000000000 ) ;
#2133=DIRECTION ( 'NONE',  ( -1.000000000000000000, 0.000000000000000000, -0.000000000000000000 ) ) ;
#2161=PRESENTATION_STYLE_ASSIGNMENT (( #8706 ) ) ;
#2320=EDGE_LOOP ( 'NONE', ( #4624, #13141 ) ) ;
#2332=DIRECTION ( 'NONE',  ( 1.000000000000000000, 0.000000000000000000, 0.000000000000000000 ) ) ;
#2545=CIRCLE ( 'NONE', #366, 18.46360580700775245 ) ;
#2571=STYLED_ITEM ( 'NONE', ( #2161 ), #2894 ) ;
#2672=DIRECTION ( 'NONE',  ( 0.000000000000000000, 0.000000000000000000, -1.000000000000000000 ) ) ;
#2694=DIRECTION ( 'NONE',  ( 0.000000000000000000, 0.000000000000000000, 1.000000000000000000 ) ) ;
#2730=VERTEX_POINT ( 'NONE', #14632 ) ;
#2812=TOROIDAL_SURFACE ( 'NONE', #7188, 22.46376988133006236, 4.000164074322307250 ) ;
#2894=MANIFOLD_SOLID_BREP ( 'Cut-Extrude1', #8831 ) ;
#2983=ORIENTED_EDGE ( 'NONE', *, *, #15479, .F. ) ;
#3099=DIRECTION ( 'NONE',  ( 0.000000000000000000, 0.000000000000000000, -1.000000000000000000 ) ) ;
#3118=EDGE_CURVE ( 'NONE', #14799, #9375, #12733, .T. ) ;
#3179=CYLINDRICAL_SURFACE ( 'NONE', #16047, 22.50000000000000000 ) ;
#3229=CYLINDRICAL_SURFACE ( 'NONE', #11074, 5.268482129199949959 ) ;
#3239=DIRECTION ( 'NONE',  ( -1.000000000000000000, -0.000000000000000000, -0.000000000000000000 ) ) ;
#3280=CARTESIAN_POINT ( 'NONE',  ( 0.000000000000000000, 0.000000000000000000, 0.000000000000000000 ) ) ;
#3293=ORIENTED_EDGE ( 'NONE', *, *, #15495, .T. ) ;
#3319=ORIENTED_EDGE ( 'NONE', *, *, #8992, .F. ) ;
#3373=ORIENTED_EDGE ( 'NONE', *, *, #8528, .T. ) ;
#3437=PLANE ( 'NONE',  #7024 ) ;
#3439=FACE_OUTER_BOUND ( 'NONE', #15641, .T. ) ;
#3440=CARTESIAN_POINT ( 'NONE',  ( -5.000000000000000000, 2.261139575227052682E-15, -18.46360580700775245 ) ) ;
#3463=FILL_AREA_STYLE ('',( #15312 ) ) ;
#3465=ORIENTED_EDGE ( 'NONE', *, *, #1703, .F. ) ;
#3518=CARTESIAN_POINT ( 'NONE',  ( 0.000000000000000000, 0.000000000000000000, 0.000000000000000000 ) ) ;
#3631=EDGE_LOOP ( 'NONE', ( #8153, #14947 ) ) ;
#3651=DIRECTION ( 'NONE',  ( -1.000000000000000000, -0.000000000000000000, -0.000000000000000000 ) ) ;
#3674=COLOUR_RGB ( '', 0.66274510, 0.83137255, 0.94901961) ;
#3740=CARTESIAN_POINT ( 'NONE',  ( -5.000000000000000000, 0.000000000000000000, 0.000000000000000000 ) ) ;
#3757=ADVANCED_FACE ( 'NONE', ( #14489 ), #5190, .T. ) ;
#3932=DIRECTION ( 'NONE',  ( 0.000000000000000000, 0.000000000000000000, 1.000000000000000000 ) ) ;
#3935=EDGE_CURVE ( 'NONE', #13578, #851, #7490, .T. ) ;
#3944=DIRECTION ( 'NONE',  ( -1.000000000000000000, -0.000000000000000000, -0.000000000000000000 ) ) ;
#3957=VECTOR ( 'NONE', #10146, 1000.000000000000000 ) ;
#3962=CARTESIAN_POINT ( 'NONE',  ( 0.000000000000000000, 0.000000000000000000, 22.50000000000000000 ) ) ;
#3988=AXIS2_PLACEMENT_3D ( 'NONE', #5475, #13223, #1708 ) ;
#3996=CARTESIAN_POINT ( 'NONE',  ( 0.000000000000000000, 0.000000000000000000, 0.000000000000000000 ) ) ;
#4039=AXIS2_PLACEMENT_3D ( 'NONE', #6040, #16442, #4668 ) ;
#4096=ORIENTED_EDGE ( 'NONE', *, *, #3118, .T. ) ;
#4114=CIRCLE ( 'NONE', #5758, 22.49999999999999645 ) ;
#4116=FACE_OUTER_BOUND ( 'NONE', #5359, .T. ) ;
#4124=FACE_BOUND ( 'NONE', #3631, .T. ) ;
#4180=CARTESIAN_POINT ( 'NONE',  ( -5.000000000000000888, 2.751018388195357790E-15, -22.46376988133006236 ) ) ;
#4209=DIRECTION ( 'NONE',  ( 0.000000000000000000, 0.000000000000000000, 1.000000000000000000 ) ) ;
#4313=FACE_OUTER_BOUND ( 'NONE', #2320, .T. ) ;
#4437=CARTESIAN_POINT ( 'NONE',  ( 0.000000000000000000, 0.000000000000000000, 0.000000000000000000 ) ) ;
#4490=AXIS2_PLACEMENT_3D ( 'NONE', #1813, #7034, #3099 ) ;
#4491=EDGE_CURVE ( 'NONE', #16266, #1294, #14122, .T. ) ;
#4545=DIRECTION ( 'NONE',  ( -1.000000000000000000, -0.000000000000000000, -0.000000000000000000 ) ) ;
#4610=CARTESIAN_POINT ( 'NONE',  ( -18.00000000000000711, 0.000000000000000000, 0.000000000000000000 ) ) ;
#4624=ORIENTED_EDGE ( 'NONE', *, *, #8992, .T. ) ;
#4627=ORIENTED_EDGE ( 'NONE', *, *, #5257, .T. ) ;
#4631=ORIENTED_EDGE ( 'NONE', *, *, #1323, .F. ) ;
#4662=EDGE_CURVE ( 'NONE', #9375, #1983, #10290, .T. ) ;
#4668=DIRECTION ( 'NONE',  ( 0.000000000000000000, 0.000000000000000000, 1.000000000000000000 ) ) ;
#4679=LINE ( 'NONE', #5976, #16535 ) ;
#4737=( LENGTH_UNIT ( ) NAMED_UNIT ( * ) SI_UNIT ( .MILLI., .METRE. ) );
#4740=ADVANCED_FACE ( 'NONE', ( #683 ), #3179, .T. ) ;
#4788=DIRECTION ( 'NONE',  ( 0.000000000000000000, 0.000000000000000000, 1.000000000000000000 ) ) ;
#4800=FACE_OUTER_BOUND ( 'NONE', #16420, .T. ) ;
#4838=DIRECTION ( 'NONE',  ( -1.000000000000000000, -0.000000000000000000, -0.000000000000000000 ) ) ;
#4861=DIRECTION ( 'NONE',  ( 0.000000000000000000, 0.000000000000000000, -1.000000000000000000 ) ) ;
#4899=CARTESIAN_POINT ( 'NONE',  ( -13.11912225705329327, 0.000000000000000000, 22.50000000000000000 ) ) ;
#4942=CARTESIAN_POINT ( 'NONE',  ( -9.000000000000001776, 0.000000000000000000, 0.000000000000000000 ) ) ;
#5005=AXIS2_PLACEMENT_3D ( 'NONE', #16144, #15963, #4209 ) ;
#5095=EDGE_CURVE ( 'NONE', #16527, #2730, #2068, .T. ) ;
#5133=DIRECTION ( 'NONE',  ( -1.000000000000000000, -0.000000000000000000, -0.000000000000000000 ) ) ;
#5144=CARTESIAN_POINT ( 'NONE',  ( -5.000000000000000000, 0.000000000000000000, 18.46360580700775245 ) ) ;
#5169=DIRECTION ( 'NONE',  ( 0.000000000000000000, 0.000000000000000000, 1.000000000000000000 ) ) ;
#5190=CYLINDRICAL_SURFACE ( 'NONE', #944, 22.50000000000000000 ) ;
#5205=DIRECTION ( 'NONE',  ( 0.000000000000000000, 0.000000000000000000, 1.000000000000000000 ) ) ;
#5257=EDGE_CURVE ( 'NONE', #386, #1641, #15237, .T. ) ;
#5344=ORIENTED_EDGE ( 'NONE', *, *, #14773, .F. ) ;
#5359=EDGE_LOOP ( 'NONE', ( #3465, #13829, #203, #10926 ) ) ;
#5475=CARTESIAN_POINT ( 'NONE',  ( 0.000000000000000000, 0.000000000000000000, 0.000000000000000000 ) ) ;
#5482=UNCERTAINTY_MEASURE_WITH_UNIT (LENGTH_MEASURE( 1.000000000000000082E-05 ), #4737, 'distance_accuracy_value', 'NONE');
#5566=DIRECTION ( 'NONE',  ( -1.000000000000000000, -0.000000000000000000, -0.000000000000000000 ) ) ;
#5738=DIRECTION ( 'NONE',  ( 0.000000000000000000, 0.000000000000000000, 1.000000000000000000 ) ) ;
#5742=ADVANCED_FACE ( 'NONE', ( #11163, #4800 ), #3437, .F. ) ;
#5758=AXIS2_PLACEMENT_3D ( 'NONE', #5968, #3239, #655 ) ;
#5786=ORIENTED_EDGE ( 'NONE', *, *, #8528, .F. ) ;
#5911=DIRECTION ( 'NONE',  ( 0.000000000000000000, 0.000000000000000000, 1.000000000000000000 ) ) ;
#5968=CARTESIAN_POINT ( 'NONE',  ( -10.00000000000000000, 0.000000000000000000, 0.000000000000000000 ) ) ;
#5976=CARTESIAN_POINT ( 'NONE',  ( -18.00000000000000711, 0.000000000000000000, -5.268482129199949959 ) ) ;
#5999=CARTESIAN_POINT ( 'NONE',  ( -5.000000000000000888, 0.000000000000000000, 22.46376988133006236 ) ) ;
#6031=LINE ( 'NONE', #8632, #1477 ) ;
#6040=CARTESIAN_POINT ( 'NONE',  ( -13.11912225705329327, 0.000000000000000000, 0.000000000000000000 ) ) ;
#6219=UNCERTAINTY_MEASURE_WITH_UNIT (LENGTH_MEASURE( 1.000000000000000082E-05 ), #14018, 'distance_accuracy_value', 'NONE');
#6372=DIRECTION ( 'NONE',  ( -1.000000000000000000, -0.000000000000000000, -0.000000000000000000 ) ) ;
#6378=VECTOR ( 'NONE', #8812, 1000.000000000000000 ) ;
#6413=CARTESIAN_POINT ( 'NONE',  ( 0.000000000000000000, 2.755455298081544778E-15, -22.50000000000000000 ) ) ;
#6417=APPLICATION_CONTEXT ( 'automotive_design' ) ;
#6561=CARTESIAN_POINT ( 'NONE',  ( -0.9999999999999991118, 0.000000000000000000, 22.50000000000000000 ) ) ;
#6564=DIRECTION ( 'NONE',  ( -1.000000000000000000, -0.000000000000000000, -0.000000000000000000 ) ) ;
#6683=TOROIDAL_SURFACE ( 'NONE', #8623, 22.46376988133006236, 4.000164074322307250 ) ;
#6692=FACE_OUTER_BOUND ( 'NONE', #13671, .T. ) ;
#6955=ORIENTED_EDGE ( 'NONE', *, *, #16425, .T. ) ;
#7022=AXIS2_PLACEMENT_3D ( 'NONE', #10213, #3944, #13049 ) ;
#7024=AXIS2_PLACEMENT_3D ( 'NONE', #3518, #2133, #9876 ) ;
#7034=DIRECTION ( 'NONE',  ( 1.000000000000000000, 0.000000000000000000, 0.000000000000000000 ) ) ;
#7056=SURFACE_SIDE_STYLE ('',( #9823 ) ) ;
#7083=DIRECTION ( 'NONE',  ( 0.000000000000000000, 0.000000000000000000, -1.000000000000000000 ) ) ;
#7105=CYLINDRICAL_SURFACE ( 'NONE', #5005, 22.50000000000000000 ) ;
#7139=ORIENTED_EDGE ( 'NONE', *, *, #15479, .T. ) ;
#7188=AXIS2_PLACEMENT_3D ( 'NONE', #11747, #1185, #5205 ) ;
#7193=DIRECTION ( 'NONE',  ( 0.000000000000000000, 0.000000000000000000, 1.000000000000000000 ) ) ;
#7201=ADVANCED_FACE ( 'NONE', ( #1032 ), #989, .F. ) ;
#7244=FACE_OUTER_BOUND ( 'NONE', #16452, .T. ) ;
#7277=ADVANCED_FACE ( 'NONE', ( #14419 ), #9780, .F. ) ;
#7368=PRODUCT_DEFINITION_SHAPE ( 'NONE', 'NONE',  #10407 ) ;
#7439=FACE_OUTER_BOUND ( 'NONE', #1029, .T. ) ;
#7490=CIRCLE ( 'NONE', #114, 5.268482129199949959 ) ;
#7567=EDGE_CURVE ( 'NONE', #8258, #14799, #2096, .T. ) ;
#7599=DIRECTION ( 'NONE',  ( 0.000000000000000000, 0.000000000000000000, 1.000000000000000000 ) ) ;
#7659=CARTESIAN_POINT ( 'NONE',  ( -10.00000000000000000, 0.000000000000000000, 0.000000000000000000 ) ) ;
#7848=LINE ( 'NONE', #15420, #6378 ) ;
#7883=ADVANCED_FACE ( 'NONE', ( #7244 ), #651, .T. ) ;
#7907=ORIENTED_EDGE ( 'NONE', *, *, #5095, .F. ) ;
#7954=CIRCLE ( 'NONE', #571, 22.50000000000000000 ) ;
#7958=APPLICATION_CONTEXT ( 'automotive_design' ) ;
#7987=SHAPE_DEFINITION_REPRESENTATION ( #7368, #11761 ) ;
#8001=ORIENTED_EDGE ( 'NONE', *, *, #12530, .F. ) ;
#8035=ORIENTED_EDGE ( 'NONE', *, *, #5257, .F. ) ;
#8153=ORIENTED_EDGE ( 'NONE', *, *, #12318, .T. ) ;
#8166=DIRECTION ( 'NONE',  ( 0.000000000000000000, 0.000000000000000000, -1.000000000000000000 ) ) ;
#8258=VERTEX_POINT ( 'NONE', #14811 ) ;
#8320=LINE ( 'NONE', #13483, #16235 ) ;
#8385=DIRECTION ( 'NONE',  ( -1.000000000000000000, -0.000000000000000000, -0.000000000000000000 ) ) ;
#8528=EDGE_CURVE ( 'NONE', #1641, #386, #13940, .T. ) ;
#8623=AXIS2_PLACEMENT_3D ( 'NONE', #13665, #15107, #7193 ) ;
#8632=CARTESIAN_POINT ( 'NONE',  ( -13.11912225705329327, 2.755455298081544778E-15, -22.50000000000000000 ) ) ;
#8693=DIRECTION ( 'NONE',  ( 0.000000000000000000, 0.000000000000000000, 1.000000000000000000 ) ) ;
#8696=ORIENTED_EDGE ( 'NONE', *, *, #842, .T. ) ;
#8706=SURFACE_STYLE_USAGE ( .BOTH. , #7056 ) ;
#8712=( NAMED_UNIT ( * ) SI_UNIT ( $, .STERADIAN. ) SOLID_ANGLE_UNIT ( ) );
#8812=DIRECTION ( 'NONE',  ( 1.000000000000000000, -0.000000000000000000, -0.000000000000000000 ) ) ;
#8831=CLOSED_SHELL ( 'NONE', ( #7201, #11186, #16749, #3757, #12338, #4740, #5742, #7883, #7277, #14496, #12189, #16311 ) ) ;
#8857=EDGE_CURVE ( 'NONE', #8258, #1983, #558, .T. ) ;
#8892=DIRECTION ( 'NONE',  ( 0.000000000000000000, 0.000000000000000000, 1.000000000000000000 ) ) ;
#8943=AXIS2_PLACEMENT_3D ( 'NONE', #12954, #5133, #10384 ) ;
#8992=EDGE_CURVE ( 'NONE', #14337, #276, #4114, .T. ) ;
#9137=CIRCLE ( 'NONE', #10503, 22.49999999999999645 ) ;
#9211=AXIS2_PLACEMENT_3D ( 'NONE', #10018, #6372, #16778 ) ;
#9293=EDGE_CURVE ( 'NONE', #1294, #16266, #7954, .T. ) ;
#9302=ORIENTED_EDGE ( 'NONE', *, *, #14773, .T. ) ;
#9375=VERTEX_POINT ( 'NONE', #5144 ) ;
#9459=DIRECTION ( 'NONE',  ( 1.000000000000000000, 0.000000000000000000, 0.000000000000000000 ) ) ;
#9563=ORIENTED_EDGE ( 'NONE', *, *, #4491, .F. ) ;
#9629=CARTESIAN_POINT ( 'NONE',  ( -10.00000000000000000, 0.000000000000000000, 0.000000000000000000 ) ) ;
#9694=ORIENTED_EDGE ( 'NONE', *, *, #4662, .F. ) ;
#9745=AXIS2_PLACEMENT_3D ( 'NONE', #4610, #10106, #4861 ) ;
#9750=( NAMED_UNIT ( * ) SI_UNIT ( $, .STERADIAN. ) SOLID_ANGLE_UNIT ( ) );
#9758=CARTESIAN_POINT ( 'NONE',  ( -10.00000000000000000, 0.000000000000000000, 22.49999999999999645 ) ) ;
#9765=CARTESIAN_POINT ( 'NONE',  ( -18.00000000000000711, 0.000000000000000000, 0.000000000000000000 ) ) ;
#9780=TOROIDAL_SURFACE ( 'NONE', #8943, 22.46376988133006236, 4.000164074322307250 ) ;
#9787=CARTESIAN_POINT ( 'NONE',  ( -10.00000000000000000, 2.755455298081544383E-15, -22.49999999999999645 ) ) ;
#9823=SURFACE_STYLE_FILL_AREA ( #3463 ) ;
#9847=CARTESIAN_POINT ( 'NONE',  ( -10.00000000000000000, 0.000000000000000000, 0.000000000000000000 ) ) ;
#9852=DIRECTION ( 'NONE',  ( 1.000000000000000000, 0.000000000000000000, 0.000000000000000000 ) ) ;
#9876=DIRECTION ( 'NONE',  ( -0.000000000000000000, 0.000000000000000000, 1.000000000000000000 ) ) ;
#9883=DIRECTION ( 'NONE',  ( 0.000000000000000000, 0.000000000000000000, -1.000000000000000000 ) ) ;
#9911=DIRECTION ( 'NONE',  ( 1.000000000000000000, 0.000000000000000000, 0.000000000000000000 ) ) ;
#9916=DIRECTION ( 'NONE',  ( 0.000000000000000000, 0.000000000000000000, -1.000000000000000000 ) ) ;
#9943=DIRECTION ( 'NONE',  ( -0.000000000000000000, 1.000000000000000000, 1.224646799147353207E-16 ) ) ;
#10018=CARTESIAN_POINT ( 'NONE',  ( -0.9999999999999991118, 0.000000000000000000, 0.000000000000000000 ) ) ;
#10106=DIRECTION ( 'NONE',  ( 1.000000000000000000, -0.000000000000000000, -0.000000000000000000 ) ) ;
#10146=DIRECTION ( 'NONE',  ( -1.000000000000000000, -0.000000000000000000, -0.000000000000000000 ) ) ;
#10194=DIRECTION ( 'NONE',  ( -1.000000000000000000, -0.000000000000000000, -0.000000000000000000 ) ) ;
#10213=CARTESIAN_POINT ( 'NONE',  ( -5.000000000000000888, 0.000000000000000000, 0.000000000000000000 ) ) ;
#10290=CIRCLE ( 'NONE', #13854, 18.46360580700775245 ) ;
#10384=DIRECTION ( 'NONE',  ( 0.000000000000000000, 0.000000000000000000, 1.000000000000000000 ) ) ;
#10407=PRODUCT_DEFINITION ( 'UNKNOWN', '', #14678, #13413 ) ;
#10464=ORIENTED_EDGE ( 'NONE', *, *, #16425, .F. ) ;
#10503=AXIS2_PLACEMENT_3D ( 'NONE', #7659, #14039, #5169 ) ;
#10541=DIRECTION ( 'NONE',  ( -1.000000000000000000, -0.000000000000000000, -0.000000000000000000 ) ) ;
#10575=AXIS2_PLACEMENT_3D ( 'NONE', #4437, #9852, #7083 ) ;
#10926=ORIENTED_EDGE ( 'NONE', *, *, #801, .F. ) ;
#11009=ORIENTED_EDGE ( 'NONE', *, *, #12318, .F. ) ;
#11074=AXIS2_PLACEMENT_3D ( 'NONE', #9765, #15149, #9916 ) ;
#11075=AXIS2_PLACEMENT_3D ( 'NONE', #12653, #9911, #16182 ) ;
#11163=FACE_BOUND ( 'NONE', #11490, .T. ) ;
#11186=ADVANCED_FACE ( 'NONE', ( #7439 ), #2812, .F. ) ;
#11220=DIRECTION ( 'NONE',  ( 1.000000000000000000, -0.000000000000000000, -0.000000000000000000 ) ) ;
#11245=DIRECTION ( 'NONE',  ( 0.000000000000000000, -1.000000000000000000, 0.000000000000000000 ) ) ;
#11268=( NAMED_UNIT ( * ) PLANE_ANGLE_UNIT ( ) SI_UNIT ( $, .RADIAN. ) );
#11334=ORIENTED_EDGE ( 'NONE', *, *, #15234, .T. ) ;
#11357=CIRCLE ( 'NONE', #1482, 4.000164074322309027 ) ;
#11490=EDGE_LOOP ( 'NONE', ( #7907, #2983 ) ) ;
#11697=AXIS2_PLACEMENT_3D ( 'NONE', #4942, #10194, #7599 ) ;
#11747=CARTESIAN_POINT ( 'NONE',  ( -5.000000000000000888, 0.000000000000000000, 0.000000000000000000 ) ) ;
#11751=DIRECTION ( 'NONE',  ( 0.000000000000000000, -1.000000000000000000, 0.000000000000000000 ) ) ;
#11761=SHAPE_REPRESENTATION ( 'Part9', ( #1488 ), #14386 ) ;
#11785=ORIENTED_EDGE ( 'NONE', *, *, #8857, .T. ) ;
#11790=ORIENTED_EDGE ( 'NONE', *, *, #12530, .T. ) ;
#11817=DIRECTION ( 'NONE',  ( 0.000000000000000000, 0.000000000000000000, 1.000000000000000000 ) ) ;
#11945=ORIENTED_EDGE ( 'NONE', *, *, #15092, .F. ) ;
#12189=ADVANCED_FACE ( 'NONE', ( #4124, #4313 ), #1467, .F. ) ;
#12199=AXIS2_PLACEMENT_3D ( 'NONE', #16456, #9943, #917 ) ;
#12280=CARTESIAN_POINT ( 'NONE',  ( -5.000000000000000000, 0.000000000000000000, 0.000000000000000000 ) ) ;
#12318=EDGE_CURVE ( 'NONE', #851, #13578, #13009, .T. ) ;
#12320=ORIENTED_EDGE ( 'NONE', *, *, #4491, .T. ) ;
#12338=ADVANCED_FACE ( 'NONE', ( #3439 ), #6683, .F. ) ;
#12445=MECHANICAL_DESIGN_GEOMETRIC_PRESENTATION_REPRESENTATION('',(#2571),#1750);
#12530=EDGE_CURVE ( 'NONE', #9375, #386, #11357, .T. ) ;
#12647=SHAPE_REPRESENTATION_RELATIONSHIP ( 'NONE' , 'NONE' ,  #11761, #15684 ) ;
#12653=CARTESIAN_POINT ( 'NONE',  ( 0.000000000000000000, 0.000000000000000000, 0.000000000000000000 ) ) ;
#12694=CIRCLE ( 'NONE', #14334, 22.50000000000000000 ) ;
#12733=CIRCLE ( 'NONE', #14929, 4.000164074322309027 ) ;
#12954=CARTESIAN_POINT ( 'NONE',  ( -5.000000000000000888, 0.000000000000000000, 0.000000000000000000 ) ) ;
#13009=CIRCLE ( 'NONE', #14097, 5.268482129199949959 ) ;
#13049=DIRECTION ( 'NONE',  ( 0.000000000000000000, 0.000000000000000000, 1.000000000000000000 ) ) ;
#13084=ORIENTED_EDGE ( 'NONE', *, *, #7567, .F. ) ;
#13141=ORIENTED_EDGE ( 'NONE', *, *, #801, .T. ) ;
#13223=DIRECTION ( 'NONE',  ( -1.000000000000000000, -0.000000000000000000, -0.000000000000000000 ) ) ;
#13413=PRODUCT_DEFINITION_CONTEXT ( 'detailed design', #6417, 'design' ) ;
#13483=CARTESIAN_POINT ( 'NONE',  ( -13.11912225705329327, 0.000000000000000000, 22.50000000000000000 ) ) ;
#13521=ORIENTED_EDGE ( 'NONE', *, *, #16048, .F. ) ;
#13578=VERTEX_POINT ( 'NONE', #15875 ) ;
#13665=CARTESIAN_POINT ( 'NONE',  ( -5.000000000000000888, 0.000000000000000000, 0.000000000000000000 ) ) ;
#13671=EDGE_LOOP ( 'NONE', ( #13688, #11009, #165, #16802 ) ) ;
#13688=ORIENTED_EDGE ( 'NONE', *, *, #15234, .F. ) ;
#13702=CARTESIAN_POINT ( 'NONE',  ( -0.9999999999999991118, 2.755455298081544778E-15, -22.50000000000000000 ) ) ;
#13818=DIRECTION ( 'NONE',  ( -1.000000000000000000, -0.000000000000000000, -0.000000000000000000 ) ) ;
#13829=ORIENTED_EDGE ( 'NONE', *, *, #7567, .T. ) ;
#13854=AXIS2_PLACEMENT_3D ( 'NONE', #12280, #13818, #4788 ) ;
#13899=CARTESIAN_POINT ( 'NONE',  ( -13.11912225705329327, 0.000000000000000000, 0.000000000000000000 ) ) ;
#13940=CIRCLE ( 'NONE', #15572, 22.50000000000000000 ) ;
#14018=( LENGTH_UNIT ( ) NAMED_UNIT ( * ) SI_UNIT ( .MILLI., .METRE. ) );
#14039=DIRECTION ( 'NONE',  ( -1.000000000000000000, -0.000000000000000000, -0.000000000000000000 ) ) ;
#14075=DIRECTION ( 'NONE',  ( 0.000000000000000000, 0.000000000000000000, -1.000000000000000000 ) ) ;
#14097=AXIS2_PLACEMENT_3D ( 'NONE', #9629, #9459, #8166 ) ;
#14122=CIRCLE ( 'NONE', #3988, 22.50000000000000000 ) ;
#14334=AXIS2_PLACEMENT_3D ( 'NONE', #1351, #10541, #3932 ) ;
#14337=VERTEX_POINT ( 'NONE', #9758 ) ;
#14386=( GEOMETRIC_REPRESENTATION_CONTEXT ( 3 ) GLOBAL_UNCERTAINTY_ASSIGNED_CONTEXT ( ( #5482 ) ) GLOBAL_UNIT_ASSIGNED_CONTEXT ( ( #4737, #11268, #8712 ) ) REPRESENTATION_CONTEXT ( 'NONE', 'WORKASPACE' ) );
#14419=FACE_OUTER_BOUND ( 'NONE', #16732, .T. ) ;
#14472=DIRECTION ( 'NONE',  ( -1.000000000000000000, -0.000000000000000000, -0.000000000000000000 ) ) ;
#14489=FACE_OUTER_BOUND ( 'NONE', #1113, .T. ) ;
#14496=ADVANCED_FACE ( 'NONE', ( #4116 ), #7105, .T. ) ;
#14632=CARTESIAN_POINT ( 'NONE',  ( 0.000000000000000000, 6.452029775889750974E-16, 5.268482129199949959 ) ) ;
#14678=PRODUCT_DEFINITION_FORMATION_WITH_SPECIFIED_SOURCE ( 'ANY', '', #1080, .NOT_KNOWN. ) ;
#14773=EDGE_CURVE ( 'NONE', #14799, #8258, #12694, .T. ) ;
#14799=VERTEX_POINT ( 'NONE', #16717 ) ;
#14811=CARTESIAN_POINT ( 'NONE',  ( -9.000000000000001776, 2.755455298081549511E-15, -22.50000000000003908 ) ) ;
#14929=AXIS2_PLACEMENT_3D ( 'NONE', #5999, #11245, #9883 ) ;
#14947=ORIENTED_EDGE ( 'NONE', *, *, #3935, .T. ) ;
#15005=EDGE_LOOP ( 'NONE', ( #4096, #374, #559, #5344 ) ) ;
#15092=EDGE_CURVE ( 'NONE', #851, #16527, #4679, .T. ) ;
#15107=DIRECTION ( 'NONE',  ( -1.000000000000000000, -0.000000000000000000, -0.000000000000000000 ) ) ;
#15149=DIRECTION ( 'NONE',  ( 1.000000000000000000, -0.000000000000000000, -0.000000000000000000 ) ) ;
#15217=DIRECTION ( 'NONE',  ( 1.000000000000000000, 0.000000000000000000, 0.000000000000000000 ) ) ;
#15234=EDGE_CURVE ( 'NONE', #13578, #2730, #7848, .T. ) ;
#15237=CIRCLE ( 'NONE', #9211, 22.50000000000000000 ) ;
#15240=CARTESIAN_POINT ( 'NONE',  ( -13.11912225705329327, 2.755455298081544778E-15, -22.50000000000000000 ) ) ;
#15312=FILL_AREA_STYLE_COLOUR ( '', #3674 ) ;
#15383=LINE ( 'NONE', #4899, #3957 ) ;
#15416=ORIENTED_EDGE ( 'NONE', *, *, #1703, .T. ) ;
#15420=CARTESIAN_POINT ( 'NONE',  ( -18.00000000000000711, 6.452029775889750974E-16, 5.268482129199949959 ) ) ;
#15479=EDGE_CURVE ( 'NONE', #2730, #16527, #1203, .T. ) ;
#15495=EDGE_CURVE ( 'NONE', #1294, #1641, #6031, .T. ) ;
#15572=AXIS2_PLACEMENT_3D ( 'NONE', #1622, #5566, #5738 ) ;
#15615=ORIENTED_EDGE ( 'NONE', *, *, #9293, .F. ) ;
#15641=EDGE_LOOP ( 'NONE', ( #1064, #6955, #3373, #8001 ) ) ;
#15684=ADVANCED_BREP_SHAPE_REPRESENTATION ( '', ( #2894, #1488 ), #14386 ) ;
#15875=CARTESIAN_POINT ( 'NONE',  ( -10.00000000000000000, 6.452029775889750974E-16, 5.268482129199949959 ) ) ;
#15935=DIRECTION ( 'NONE',  ( -0.000000000000000000, 1.000000000000000000, 1.224646799147353207E-16 ) ) ;
#15963=DIRECTION ( 'NONE',  ( -1.000000000000000000, -0.000000000000000000, -0.000000000000000000 ) ) ;
#15993=EDGE_LOOP ( 'NONE', ( #12320, #3293, #8035, #13521 ) ) ;
#16033=DIRECTION ( 'NONE',  ( 0.000000000000000000, -1.224646799147352714E-16, 1.000000000000000000 ) ) ;
#16047=AXIS2_PLACEMENT_3D ( 'NONE', #13899, #4545, #5911 ) ;
#16048=EDGE_CURVE ( 'NONE', #16266, #386, #15383, .T. ) ;
#16101=ORIENTED_EDGE ( 'NONE', *, *, #3118, .F. ) ;
#16144=CARTESIAN_POINT ( 'NONE',  ( -13.11912225705329327, 0.000000000000000000, 0.000000000000000000 ) ) ;
#16182=DIRECTION ( 'NONE',  ( 0.000000000000000000, 0.000000000000000000, -1.000000000000000000 ) ) ;
#16235=VECTOR ( 'NONE', #431, 1000.000000000000000 ) ;
#16266=VERTEX_POINT ( 'NONE', #3962 ) ;
#16311=ADVANCED_FACE ( 'NONE', ( #6692 ), #184, .F. ) ;
#16313=CIRCLE ( 'NONE', #12199, 4.000164074322309027 ) ;
#16408=VECTOR ( 'NONE', #4838, 1000.000000000000000 ) ;
#16420=EDGE_LOOP ( 'NONE', ( #9563, #15615 ) ) ;
#16425=EDGE_CURVE ( 'NONE', #1983, #1641, #16313, .T. ) ;
#16442=DIRECTION ( 'NONE',  ( -1.000000000000000000, -0.000000000000000000, -0.000000000000000000 ) ) ;
#16452=EDGE_LOOP ( 'NONE', ( #105, #1278, #468, #5786 ) ) ;
#16456=CARTESIAN_POINT ( 'NONE',  ( -5.000000000000000888, 2.751018388195357790E-15, -22.46376988133006236 ) ) ;
#16457=AXIS2_PLACEMENT_3D ( 'NONE', #4180, #15935, #16033 ) ;
#16527=VERTEX_POINT ( 'NONE', #1253 ) ;
#16535=VECTOR ( 'NONE', #11220, 1000.000000000000000 ) ;
#16636=ORIENTED_EDGE ( 'NONE', *, *, #3935, .F. ) ;
#16717=CARTESIAN_POINT ( 'NONE',  ( -9.000000000000001776, 0.000000000000000000, 22.50000000000003908 ) ) ;
#16732=EDGE_LOOP ( 'NONE', ( #9694, #11790, #4627, #10464 ) ) ;
#16749=ADVANCED_FACE ( 'NONE', ( #1853 ), #3229, .F. ) ;
#16778=DIRECTION ( 'NONE',  ( 0.000000000000000000, 0.000000000000000000, 1.000000000000000000 ) ) ;
#16802=ORIENTED_EDGE ( 'NONE', *, *, #5095, .T. ) ;
ENDSEC;
END-ISO-10303-21;
